ISO-10303-21;
HEADER;
/* Generated by software containing ST-Developer
 * from STEP Tools, Inc. (www.steptools.com) 
 */

FILE_DESCRIPTION(
/* description */ ('Flywheel Crank-Slider'),
/* implementation_level */ '2;1');

FILE_NAME(
/* name */ 'Bearing bolt reducer (2).step',
/* time_stamp */ '2026-10-28T03:23:13-07:00',
/* author */ (''),
/* organization */ (''),
/* preprocessor_version */ 'ST-DEVELOPER v20.2',
/* originating_system */ 'Autodesk Translation Framework v15.17.0.0',
/* authorisation */ '');

FILE_SCHEMA (('AUTOMOTIVE_DESIGN { 1 0 10303 214 3 1 1 }'));
ENDSEC;

DATA;
#10=MECHANICAL_DESIGN_GEOMETRIC_PRESENTATION_REPRESENTATION('',(#673),#17322);
#569=SHAPE_REPRESENTATION_RELATIONSHIP('SRR','None',#17565,#621);
#621=ADVANCED_BREP_SHAPE_REPRESENTATION('',(#734),#17269);
#673=STYLED_ITEM('',(#17938),#734);
#734=MANIFOLD_SOLID_BREP('Body1',#9051);
#841=FACE_BOUND('',#1984,.T.);
#842=FACE_BOUND('',#1986,.T.);
#1045=PLANE('',#9841);
#1046=PLANE('',#9842);
#1390=FACE_OUTER_BOUND('',#1981,.T.);
#1391=FACE_OUTER_BOUND('',#1982,.T.);
#1392=FACE_OUTER_BOUND('',#1983,.T.);
#1393=FACE_OUTER_BOUND('',#1985,.T.);
#1981=EDGE_LOOP('',(#6410,#6411,#6412,#6413));
#1982=EDGE_LOOP('',(#6414,#6415,#6416,#6417));
#1983=EDGE_LOOP('',(#6418));
#1984=EDGE_LOOP('',(#6419));
#1985=EDGE_LOOP('',(#6420));
#1986=EDGE_LOOP('',(#6421));
#2688=LINE('',#14053,#3299);
#2689=LINE('',#14059,#3300);
#3299=VECTOR('',#11206,0.425);
#3300=VECTOR('',#11213,0.645);
#3910=CIRCLE('',#9836,0.425);
#3911=CIRCLE('',#9837,0.425);
#3912=CIRCLE('',#9839,0.645);
#3913=CIRCLE('',#9840,0.645);
#4373=VERTEX_POINT('',#14050);
#4374=VERTEX_POINT('',#14052);
#4375=VERTEX_POINT('',#14056);
#4376=VERTEX_POINT('',#14058);
#5162=EDGE_CURVE('',#4373,#4373,#3910,.T.);
#5163=EDGE_CURVE('',#4373,#4374,#2688,.T.);
#5164=EDGE_CURVE('',#4374,#4374,#3911,.T.);
#5165=EDGE_CURVE('',#4375,#4375,#3912,.T.);
#5166=EDGE_CURVE('',#4375,#4376,#2689,.T.);
#5167=EDGE_CURVE('',#4376,#4376,#3913,.T.);
#6410=ORIENTED_EDGE('',*,*,#5162,.F.);
#6411=ORIENTED_EDGE('',*,*,#5163,.T.);
#6412=ORIENTED_EDGE('',*,*,#5164,.T.);
#6413=ORIENTED_EDGE('',*,*,#5163,.F.);
#6414=ORIENTED_EDGE('',*,*,#5165,.F.);
#6415=ORIENTED_EDGE('',*,*,#5166,.T.);
#6416=ORIENTED_EDGE('',*,*,#5167,.T.);
#6417=ORIENTED_EDGE('',*,*,#5166,.F.);
#6418=ORIENTED_EDGE('',*,*,#5165,.T.);
#6419=ORIENTED_EDGE('',*,*,#5162,.T.);
#6420=ORIENTED_EDGE('',*,*,#5167,.F.);
#6421=ORIENTED_EDGE('',*,*,#5164,.F.);
#8366=CYLINDRICAL_SURFACE('',#9835,0.425);
#8367=CYLINDRICAL_SURFACE('',#9838,0.645);
#8581=ADVANCED_FACE('',(#1390),#8366,.F.);
#8582=ADVANCED_FACE('',(#1391),#8367,.T.);
#8583=ADVANCED_FACE('',(#1392,#841),#1045,.T.);
#8584=ADVANCED_FACE('',(#1393,#842),#1046,.F.);
#9051=CLOSED_SHELL('',(#8581,#8582,#8583,#8584));
#9834=AXIS2_PLACEMENT_3D('',#14048,#11200,#11201);
#9835=AXIS2_PLACEMENT_3D('',#14049,#11202,#11203);
#9836=AXIS2_PLACEMENT_3D('',#14051,#11204,#11205);
#9837=AXIS2_PLACEMENT_3D('',#14054,#11207,#11208);
#9838=AXIS2_PLACEMENT_3D('',#14055,#11209,#11210);
#9839=AXIS2_PLACEMENT_3D('',#14057,#11211,#11212);
#9840=AXIS2_PLACEMENT_3D('',#14060,#11214,#11215);
#9841=AXIS2_PLACEMENT_3D('',#14061,#11216,#11217);
#9842=AXIS2_PLACEMENT_3D('',#14062,#11218,#11219);
#11200=DIRECTION('axis',(0.,0.,1.));
#11201=DIRECTION('refdir',(1.,0.,0.));
#11202=DIRECTION('center_axis',(0.,0.,1.));
#11203=DIRECTION('ref_axis',(1.,0.,0.));
#11204=DIRECTION('center_axis',(0.,0.,-1.));
#11205=DIRECTION('ref_axis',(1.,0.,0.));
#11206=DIRECTION('',(0.,0.,-1.));
#11207=DIRECTION('center_axis',(0.,0.,-1.));
#11208=DIRECTION('ref_axis',(1.,0.,0.));
#11209=DIRECTION('center_axis',(0.,0.,1.));
#11210=DIRECTION('ref_axis',(1.,0.,0.));
#11211=DIRECTION('center_axis',(0.,0.,1.));
#11212=DIRECTION('ref_axis',(1.,0.,0.));
#11213=DIRECTION('',(0.,0.,-1.));
#11214=DIRECTION('center_axis',(0.,0.,1.));
#11215=DIRECTION('ref_axis',(1.,0.,0.));
#11216=DIRECTION('center_axis',(0.,0.,1.));
#11217=DIRECTION('ref_axis',(1.,0.,0.));
#11218=DIRECTION('center_axis',(0.,0.,1.));
#11219=DIRECTION('ref_axis',(1.,0.,0.));
#14048=CARTESIAN_POINT('',(0.,0.,0.));
#14049=CARTESIAN_POINT('Origin',(-4.75,-7.,6.67));
#14050=CARTESIAN_POINT('',(-5.175,-7.,7.87));
#14051=CARTESIAN_POINT('Origin',(-4.75,-7.,7.87));
#14052=CARTESIAN_POINT('',(-5.175,-7.,6.67));
#14053=CARTESIAN_POINT('',(-5.175,-7.,6.67));
#14054=CARTESIAN_POINT('Origin',(-4.75,-7.,6.67));
#14055=CARTESIAN_POINT('Origin',(-4.75,-7.,6.67));
#14056=CARTESIAN_POINT('',(-5.395,-7.,7.87));
#14057=CARTESIAN_POINT('Origin',(-4.75,-7.,7.87));
#14058=CARTESIAN_POINT('',(-5.395,-7.,6.67));
#14059=CARTESIAN_POINT('',(-5.395,-7.,6.67));
#14060=CARTESIAN_POINT('Origin',(-4.75,-7.,6.67));
#14061=CARTESIAN_POINT('Origin',(-4.75,-7.,7.87));
#14062=CARTESIAN_POINT('Origin',(-4.75,-7.,6.67));
#17208=UNCERTAINTY_MEASURE_WITH_UNIT(LENGTH_MEASURE(0.001),#17323,
'DISTANCE_ACCURACY_VALUE',
'Maximum model space distance between geometric entities at asserted c
onnectivities');
#17261=UNCERTAINTY_MEASURE_WITH_UNIT(LENGTH_MEASURE(0.001),#17323,
'DISTANCE_ACCURACY_VALUE',
'Maximum model space distance between geometric entities at asserted c
onnectivities');
#17269=(
GEOMETRIC_REPRESENTATION_CONTEXT(3)
GLOBAL_UNCERTAINTY_ASSIGNED_CONTEXT((#17208))
GLOBAL_UNIT_ASSIGNED_CONTEXT((#17323,#17325,#17326))
REPRESENTATION_CONTEXT('','3D')
);
#17322=(
GEOMETRIC_REPRESENTATION_CONTEXT(3)
GLOBAL_UNCERTAINTY_ASSIGNED_CONTEXT((#17261))
GLOBAL_UNIT_ASSIGNED_CONTEXT((#17323,#17325,#17326))
REPRESENTATION_CONTEXT('','3D')
);
#17323=(
LENGTH_UNIT()
NAMED_UNIT(*)
SI_UNIT(.CENTI.,.METRE.)
);
#17325=(
NAMED_UNIT(*)
PLANE_ANGLE_UNIT()
SI_UNIT($,.RADIAN.)
);
#17326=(
NAMED_UNIT(*)
SI_UNIT($,.STERADIAN.)
SOLID_ANGLE_UNIT()
);
#17334=SHAPE_DEFINITION_REPRESENTATION(#17394,#17565);
#17394=PRODUCT_DEFINITION_SHAPE('',$,#17626);
#17565=SHAPE_REPRESENTATION('',(#9834),#17269);
#17618=PRODUCT_DEFINITION_CONTEXT('part definition',#17800,'design');
#17626=PRODUCT_DEFINITION('Bearing bolt reducer (2)',
'Bearing bolt reducer (2)',#17686,#17618);
#17686=PRODUCT_DEFINITION_FORMATION('',$,#17809);
#17800=APPLICATION_CONTEXT(
'Core Data for Automotive Mechanical Design Process');
#17801=PRODUCT_CONTEXT('part definition',#17800,'mechanical');
#17809=PRODUCT('Bearing bolt reducer (2)','Bearing bolt reducer (2)',
'Bearing bolt reducer (2)',(#17801));
#17932=COLOUR_RGB('Black',0.12,0.14,0.17);
#17933=FILL_AREA_STYLE_COLOUR('',#17932);
#17934=FILL_AREA_STYLE('',(#17933));
#17935=SURFACE_STYLE_FILL_AREA(#17934);
#17936=SURFACE_SIDE_STYLE('',(#17935));
#17937=SURFACE_STYLE_USAGE(.BOTH.,#17936);
#17938=PRESENTATION_STYLE_ASSIGNMENT((#17937));
ENDSEC;
END-ISO-10303-21;
